ISO-10303-21;
HEADER;
/* Generated by software containing ST-Developer
 * from STEP Tools, Inc. (www.steptools.com) 
 */

FILE_DESCRIPTION(
/* description */ ('Ball-type isolation valve (generic)'),
/* implementation_level */ '2;1');

FILE_NAME(
/* name */ 'Bridge spacer (3).step',
/* time_stamp */ '2026-10-27T10:53:05-07:00',
/* author */ (''),
/* organization */ (''),
/* preprocessor_version */ 'ST-DEVELOPER v20.2',
/* originating_system */ 'Autodesk Translation Framework v15.17.0.0',
/* authorisation */ '');

FILE_SCHEMA (('AUTOMOTIVE_DESIGN { 1 0 10303 214 3 1 1 }'));
ENDSEC;

DATA;
#10=MECHANICAL_DESIGN_GEOMETRIC_PRESENTATION_REPRESENTATION('',(#289),#7425);
#237=SHAPE_REPRESENTATION_RELATIONSHIP('SRR','None',#7547,#263);
#263=ADVANCED_BREP_SHAPE_REPRESENTATION('',(#315),#7410);
#289=STYLED_ITEM('',(#7737),#315);
#315=MANIFOLD_SOLID_BREP('Body1',#4094);
#397=FACE_BOUND('',#1005,.T.);
#398=FACE_BOUND('',#1007,.T.);
#476=PLANE('',#4629);
#477=PLANE('',#4630);
#687=FACE_OUTER_BOUND('',#1002,.T.);
#688=FACE_OUTER_BOUND('',#1003,.T.);
#689=FACE_OUTER_BOUND('',#1004,.T.);
#690=FACE_OUTER_BOUND('',#1006,.T.);
#1002=EDGE_LOOP('',(#3213,#3214,#3215,#3216));
#1003=EDGE_LOOP('',(#3217,#3218,#3219,#3220));
#1004=EDGE_LOOP('',(#3221));
#1005=EDGE_LOOP('',(#3222));
#1006=EDGE_LOOP('',(#3223));
#1007=EDGE_LOOP('',(#3224));
#1282=LINE('',#6693,#1590);
#1283=LINE('',#6699,#1591);
#1590=VECTOR('',#5467,0.225);
#1591=VECTOR('',#5474,0.4);
#1883=CIRCLE('',#4624,0.225);
#1884=CIRCLE('',#4625,0.225);
#1885=CIRCLE('',#4627,0.4);
#1886=CIRCLE('',#4628,0.4);
#2103=VERTEX_POINT('',#6690);
#2104=VERTEX_POINT('',#6692);
#2105=VERTEX_POINT('',#6696);
#2106=VERTEX_POINT('',#6698);
#2499=EDGE_CURVE('',#2103,#2103,#1883,.T.);
#2500=EDGE_CURVE('',#2103,#2104,#1282,.T.);
#2501=EDGE_CURVE('',#2104,#2104,#1884,.T.);
#2502=EDGE_CURVE('',#2105,#2105,#1885,.T.);
#2503=EDGE_CURVE('',#2105,#2106,#1283,.T.);
#2504=EDGE_CURVE('',#2106,#2106,#1886,.T.);
#3213=ORIENTED_EDGE('',*,*,#2499,.F.);
#3214=ORIENTED_EDGE('',*,*,#2500,.T.);
#3215=ORIENTED_EDGE('',*,*,#2501,.T.);
#3216=ORIENTED_EDGE('',*,*,#2500,.F.);
#3217=ORIENTED_EDGE('',*,*,#2502,.F.);
#3218=ORIENTED_EDGE('',*,*,#2503,.T.);
#3219=ORIENTED_EDGE('',*,*,#2504,.T.);
#3220=ORIENTED_EDGE('',*,*,#2503,.F.);
#3221=ORIENTED_EDGE('',*,*,#2502,.T.);
#3222=ORIENTED_EDGE('',*,*,#2499,.T.);
#3223=ORIENTED_EDGE('',*,*,#2504,.F.);
#3224=ORIENTED_EDGE('',*,*,#2501,.F.);
#3811=CYLINDRICAL_SURFACE('',#4623,0.225);
#3812=CYLINDRICAL_SURFACE('',#4626,0.4);
#3941=ADVANCED_FACE('',(#687),#3811,.F.);
#3942=ADVANCED_FACE('',(#688),#3812,.T.);
#3943=ADVANCED_FACE('',(#689,#397),#476,.T.);
#3944=ADVANCED_FACE('',(#690,#398),#477,.F.);
#4094=CLOSED_SHELL('',(#3941,#3942,#3943,#3944));
#4622=AXIS2_PLACEMENT_3D('',#6688,#5461,#5462);
#4623=AXIS2_PLACEMENT_3D('',#6689,#5463,#5464);
#4624=AXIS2_PLACEMENT_3D('',#6691,#5465,#5466);
#4625=AXIS2_PLACEMENT_3D('',#6694,#5468,#5469);
#4626=AXIS2_PLACEMENT_3D('',#6695,#5470,#5471);
#4627=AXIS2_PLACEMENT_3D('',#6697,#5472,#5473);
#4628=AXIS2_PLACEMENT_3D('',#6700,#5475,#5476);
#4629=AXIS2_PLACEMENT_3D('',#6701,#5477,#5478);
#4630=AXIS2_PLACEMENT_3D('',#6702,#5479,#5480);
#5461=DIRECTION('axis',(0.,0.,1.));
#5462=DIRECTION('refdir',(1.,0.,0.));
#5463=DIRECTION('center_axis',(0.,0.,1.));
#5464=DIRECTION('ref_axis',(1.,0.,0.));
#5465=DIRECTION('center_axis',(0.,0.,-1.));
#5466=DIRECTION('ref_axis',(1.,0.,0.));
#5467=DIRECTION('',(0.,0.,-1.));
#5468=DIRECTION('center_axis',(0.,0.,-1.));
#5469=DIRECTION('ref_axis',(1.,0.,0.));
#5470=DIRECTION('center_axis',(0.,0.,1.));
#5471=DIRECTION('ref_axis',(1.,0.,0.));
#5472=DIRECTION('center_axis',(0.,0.,1.));
#5473=DIRECTION('ref_axis',(1.,0.,0.));
#5474=DIRECTION('',(0.,0.,-1.));
#5475=DIRECTION('center_axis',(0.,0.,1.));
#5476=DIRECTION('ref_axis',(1.,0.,0.));
#5477=DIRECTION('center_axis',(0.,0.,1.));
#5478=DIRECTION('ref_axis',(1.,0.,0.));
#5479=DIRECTION('center_axis',(0.,0.,1.));
#5480=DIRECTION('ref_axis',(1.,0.,0.));
#6688=CARTESIAN_POINT('',(0.,0.,0.));
#6689=CARTESIAN_POINT('Origin',(1.3,1.,7.5));
#6690=CARTESIAN_POINT('',(1.075,1.,8.));
#6691=CARTESIAN_POINT('Origin',(1.3,1.,8.));
#6692=CARTESIAN_POINT('',(1.075,1.,7.5));
#6693=CARTESIAN_POINT('',(1.075,1.,7.5));
#6694=CARTESIAN_POINT('Origin',(1.3,1.,7.5));
#6695=CARTESIAN_POINT('Origin',(1.3,1.,7.5));
#6696=CARTESIAN_POINT('',(0.9,1.,8.));
#6697=CARTESIAN_POINT('Origin',(1.3,1.,8.));
#6698=CARTESIAN_POINT('',(0.9,1.,7.5));
#6699=CARTESIAN_POINT('',(0.9,1.,7.5));
#6700=CARTESIAN_POINT('Origin',(1.3,1.,7.5));
#6701=CARTESIAN_POINT('Origin',(1.3,1.,8.));
#6702=CARTESIAN_POINT('Origin',(1.3,1.,7.5));
#7380=UNCERTAINTY_MEASURE_WITH_UNIT(LENGTH_MEASURE(0.001),#7426,
'DISTANCE_ACCURACY_VALUE',
'Maximum model space distance between geometric entities at asserted c
onnectivities');
#7395=UNCERTAINTY_MEASURE_WITH_UNIT(LENGTH_MEASURE(0.001),#7426,
'DISTANCE_ACCURACY_VALUE',
'Maximum model space distance between geometric entities at asserted c
onnectivities');
#7410=(
GEOMETRIC_REPRESENTATION_CONTEXT(3)
GLOBAL_UNCERTAINTY_ASSIGNED_CONTEXT((#7380))
GLOBAL_UNIT_ASSIGNED_CONTEXT((#7426,#7428,#7429))
REPRESENTATION_CONTEXT('','3D')
);
#7425=(
GEOMETRIC_REPRESENTATION_CONTEXT(3)
GLOBAL_UNCERTAINTY_ASSIGNED_CONTEXT((#7395))
GLOBAL_UNIT_ASSIGNED_CONTEXT((#7426,#7428,#7429))
REPRESENTATION_CONTEXT('','3D')
);
#7426=(
LENGTH_UNIT()
NAMED_UNIT(*)
SI_UNIT(.CENTI.,.METRE.)
);
#7428=(
NAMED_UNIT(*)
PLANE_ANGLE_UNIT()
SI_UNIT($,.RADIAN.)
);
#7429=(
NAMED_UNIT(*)
SI_UNIT($,.STERADIAN.)
SOLID_ANGLE_UNIT()
);
#7444=SHAPE_DEFINITION_REPRESENTATION(#7473,#7547);
#7473=PRODUCT_DEFINITION_SHAPE('',$,#7577);
#7547=SHAPE_REPRESENTATION('',(#4622),#7410);
#7562=PRODUCT_DEFINITION_CONTEXT('part definition',#7651,'design');
#7577=PRODUCT_DEFINITION('Bridge spacer (3)','Bridge spacer (3)',#7606,#7562);
#7606=PRODUCT_DEFINITION_FORMATION('',$,#7667);
#7651=APPLICATION_CONTEXT(
'Core Data for Automotive Mechanical Design Process');
#7652=PRODUCT_CONTEXT('part definition',#7651,'mechanical');
#7667=PRODUCT('Bridge spacer (3)','Bridge spacer (3)','Bridge spacer (3)',(#7652));
#7731=COLOUR_RGB('Sky Blue',0.24,0.69,0.87);
#7732=FILL_AREA_STYLE_COLOUR('',#7731);
#7733=FILL_AREA_STYLE('',(#7732));
#7734=SURFACE_STYLE_FILL_AREA(#7733);
#7735=SURFACE_SIDE_STYLE('',(#7734));
#7736=SURFACE_STYLE_USAGE(.BOTH.,#7735);
#7737=PRESENTATION_STYLE_ASSIGNMENT((#7736));
ENDSEC;
END-ISO-10303-21;
